ISO-10303-21;
HEADER;
/* Generated by software containing ST-Developer
 * from STEP Tools, Inc. (www.steptools.com) 
 */

FILE_DESCRIPTION(
/* description */ (''),
/* implementation_level */ '2;1');

FILE_NAME(
/* name */ 'Front_Plate.step',
/* time_stamp */ '2026-10-23T22:28:14+06:00',
/* author */ (''),
/* organization */ (''),
/* preprocessor_version */ 'ST-DEVELOPER v20.2',
/* originating_system */ 'Autodesk Translation Framework v15.15.0.0',
/* authorisation */ '');

FILE_SCHEMA (('AUTOMOTIVE_DESIGN { 1 0 10303 214 3 1 1 }'));
ENDSEC;

DATA;
#10=MECHANICAL_DESIGN_GEOMETRIC_PRESENTATION_REPRESENTATION('',(#106),#6753);
#80=SHAPE_REPRESENTATION_RELATIONSHIP('SRR','None',#6803,#93);
#93=ADVANCED_BREP_SHAPE_REPRESENTATION('',(#119),#6743);
#106=STYLED_ITEM('',(#6935),#119);
#119=MANIFOLD_SOLID_BREP('Front_Plate',#3755);
#134=FACE_BOUND('',#580,.T.);
#135=FACE_BOUND('',#582,.T.);
#136=FACE_BOUND('',#601,.T.);
#137=FACE_BOUND('',#602,.T.);
#138=FACE_BOUND('',#603,.T.);
#139=FACE_BOUND('',#604,.T.);
#140=FACE_BOUND('',#605,.T.);
#141=FACE_BOUND('',#606,.T.);
#142=FACE_BOUND('',#607,.T.);
#143=FACE_BOUND('',#608,.T.);
#144=FACE_BOUND('',#609,.T.);
#145=FACE_BOUND('',#610,.T.);
#146=FACE_BOUND('',#611,.T.);
#147=FACE_BOUND('',#612,.T.);
#148=FACE_BOUND('',#613,.T.);
#149=FACE_BOUND('',#614,.T.);
#150=FACE_BOUND('',#615,.T.);
#151=FACE_BOUND('',#616,.T.);
#152=FACE_BOUND('',#617,.T.);
#153=FACE_BOUND('',#619,.T.);
#154=FACE_BOUND('',#620,.T.);
#155=FACE_BOUND('',#621,.T.);
#156=FACE_BOUND('',#622,.T.);
#157=FACE_BOUND('',#623,.T.);
#158=FACE_BOUND('',#624,.T.);
#159=FACE_BOUND('',#625,.T.);
#160=FACE_BOUND('',#626,.T.);
#161=FACE_BOUND('',#627,.T.);
#162=FACE_BOUND('',#628,.T.);
#163=FACE_BOUND('',#629,.T.);
#164=FACE_BOUND('',#630,.T.);
#165=FACE_BOUND('',#631,.T.);
#166=FACE_BOUND('',#632,.T.);
#167=FACE_BOUND('',#633,.T.);
#168=FACE_BOUND('',#634,.T.);
#169=FACE_BOUND('',#635,.T.);
#200=PLANE('',#3961);
#201=PLANE('',#3964);
#202=PLANE('',#3965);
#203=PLANE('',#3974);
#204=PLANE('',#4026);
#205=PLANE('',#4027);
#357=FACE_OUTER_BOUND('',#575,.T.);
#358=FACE_OUTER_BOUND('',#576,.T.);
#359=FACE_OUTER_BOUND('',#577,.T.);
#360=FACE_OUTER_BOUND('',#578,.T.);
#361=FACE_OUTER_BOUND('',#579,.T.);
#362=FACE_OUTER_BOUND('',#581,.T.);
#363=FACE_OUTER_BOUND('',#583,.T.);
#364=FACE_OUTER_BOUND('',#584,.T.);
#365=FACE_OUTER_BOUND('',#585,.T.);
#366=FACE_OUTER_BOUND('',#586,.T.);
#367=FACE_OUTER_BOUND('',#587,.T.);
#368=FACE_OUTER_BOUND('',#588,.T.);
#369=FACE_OUTER_BOUND('',#589,.T.);
#370=FACE_OUTER_BOUND('',#590,.T.);
#371=FACE_OUTER_BOUND('',#591,.T.);
#372=FACE_OUTER_BOUND('',#592,.T.);
#373=FACE_OUTER_BOUND('',#593,.T.);
#374=FACE_OUTER_BOUND('',#594,.T.);
#375=FACE_OUTER_BOUND('',#595,.T.);
#376=FACE_OUTER_BOUND('',#596,.T.);
#377=FACE_OUTER_BOUND('',#597,.T.);
#378=FACE_OUTER_BOUND('',#598,.T.);
#379=FACE_OUTER_BOUND('',#599,.T.);
#380=FACE_OUTER_BOUND('',#600,.T.);
#381=FACE_OUTER_BOUND('',#618,.T.);
#575=EDGE_LOOP('',(#2548,#2549,#2550,#2551));
#576=EDGE_LOOP('',(#2552,#2553,#2554,#2555));
#577=EDGE_LOOP('',(#2556,#2557,#2558,#2559));
#578=EDGE_LOOP('',(#2560,#2561,#2562,#2563,#2564,#2565,#2566,#2567));
#579=EDGE_LOOP('',(#2568,#2569,#2570,#2571));
#580=EDGE_LOOP('',(#2572,#2573,#2574,#2575));
#581=EDGE_LOOP('',(#2576));
#582=EDGE_LOOP('',(#2577));
#583=EDGE_LOOP('',(#2578,#2579,#2580,#2581));
#584=EDGE_LOOP('',(#2582,#2583,#2584,#2585));
#585=EDGE_LOOP('',(#2586,#2587,#2588,#2589));
#586=EDGE_LOOP('',(#2590,#2591,#2592,#2593));
#587=EDGE_LOOP('',(#2594,#2595,#2596,#2597));
#588=EDGE_LOOP('',(#2598,#2599,#2600,#2601));
#589=EDGE_LOOP('',(#2602,#2603,#2604,#2605));
#590=EDGE_LOOP('',(#2606,#2607,#2608,#2609));
#591=EDGE_LOOP('',(#2610,#2611,#2612,#2613));
#592=EDGE_LOOP('',(#2614,#2615,#2616,#2617));
#593=EDGE_LOOP('',(#2618,#2619,#2620,#2621));
#594=EDGE_LOOP('',(#2622,#2623,#2624,#2625));
#595=EDGE_LOOP('',(#2626,#2627,#2628,#2629));
#596=EDGE_LOOP('',(#2630,#2631,#2632,#2633));
#597=EDGE_LOOP('',(#2634,#2635,#2636,#2637));
#598=EDGE_LOOP('',(#2638,#2639,#2640,#2641));
#599=EDGE_LOOP('',(#2642,#2643,#2644,#2645));
#600=EDGE_LOOP('',(#2646));
#601=EDGE_LOOP('',(#2647));
#602=EDGE_LOOP('',(#2648));
#603=EDGE_LOOP('',(#2649));
#604=EDGE_LOOP('',(#2650));
#605=EDGE_LOOP('',(#2651));
#606=EDGE_LOOP('',(#2652));
#607=EDGE_LOOP('',(#2653));
#608=EDGE_LOOP('',(#2654));
#609=EDGE_LOOP('',(#2655));
#610=EDGE_LOOP('',(#2656));
#611=EDGE_LOOP('',(#2657));
#612=EDGE_LOOP('',(#2658));
#613=EDGE_LOOP('',(#2659));
#614=EDGE_LOOP('',(#2660));
#615=EDGE_LOOP('',(#2661));
#616=EDGE_LOOP('',(#2662));
#617=EDGE_LOOP('',(#2663));
#618=EDGE_LOOP('',(#2664,#2665,#2666,#2667,#2668));
#619=EDGE_LOOP('',(#2669));
#620=EDGE_LOOP('',(#2670));
#621=EDGE_LOOP('',(#2671));
#622=EDGE_LOOP('',(#2672));
#623=EDGE_LOOP('',(#2673));
#624=EDGE_LOOP('',(#2674));
#625=EDGE_LOOP('',(#2675));
#626=EDGE_LOOP('',(#2676));
#627=EDGE_LOOP('',(#2677));
#628=EDGE_LOOP('',(#2678));
#629=EDGE_LOOP('',(#2679));
#630=EDGE_LOOP('',(#2680));
#631=EDGE_LOOP('',(#2681));
#632=EDGE_LOOP('',(#2682));
#633=EDGE_LOOP('',(#2683));
#634=EDGE_LOOP('',(#2684));
#635=EDGE_LOOP('',(#2685));
#839=CIRCLE('',#3962,34.);
#840=CIRCLE('',#3963,35.);
#841=CIRCLE('',#3967,34.);
#842=CIRCLE('',#3968,34.);
#843=CIRCLE('',#3969,34.);
#844=CIRCLE('',#3971,35.);
#845=CIRCLE('',#3972,35.);
#846=CIRCLE('',#3973,35.);
#847=CIRCLE('',#3976,1.1);
#848=CIRCLE('',#3977,1.1);
#849=CIRCLE('',#3979,1.1);
#850=CIRCLE('',#3980,1.1);
#851=CIRCLE('',#3982,25.);
#852=CIRCLE('',#3983,25.);
#853=CIRCLE('',#3985,1.1);
#854=CIRCLE('',#3986,1.1);
#855=CIRCLE('',#3988,1.1);
#856=CIRCLE('',#3989,1.1);
#857=CIRCLE('',#3991,1.1);
#858=CIRCLE('',#3992,1.1);
#859=CIRCLE('',#3994,1.1);
#860=CIRCLE('',#3995,1.1);
#861=CIRCLE('',#3997,1.1);
#862=CIRCLE('',#3998,1.1);
#863=CIRCLE('',#4000,1.1);
#864=CIRCLE('',#4001,1.1);
#865=CIRCLE('',#4003,1.1);
#866=CIRCLE('',#4004,1.1);
#867=CIRCLE('',#4006,1.1);
#868=CIRCLE('',#4007,1.1);
#869=CIRCLE('',#4009,1.1);
#870=CIRCLE('',#4010,1.1);
#871=CIRCLE('',#4012,1.1);
#872=CIRCLE('',#4013,1.1);
#873=CIRCLE('',#4015,1.1);
#874=CIRCLE('',#4016,1.1);
#875=CIRCLE('',#4018,1.1);
#876=CIRCLE('',#4019,1.1);
#877=CIRCLE('',#4021,1.1);
#878=CIRCLE('',#4022,1.1);
#879=CIRCLE('',#4024,1.1);
#880=CIRCLE('',#4025,1.1);
#1055=LINE('',#5674,#1341);
#1056=LINE('',#5677,#1342);
#1057=LINE('',#5680,#1343);
#1058=LINE('',#5682,#1344);
#1059=LINE('',#5683,#1345);
#1060=LINE('',#5686,#1346);
#1061=LINE('',#5688,#1347);
#1062=LINE('',#5689,#1348);
#1063=LINE('',#5694,#1349);
#1064=LINE('',#5701,#1350);
#1065=LINE('',#5709,#1351);
#1066=LINE('',#5715,#1352);
#1067=LINE('',#5721,#1353);
#1068=LINE('',#5727,#1354);
#1069=LINE('',#5733,#1355);
#1070=LINE('',#5739,#1356);
#1071=LINE('',#5745,#1357);
#1072=LINE('',#5751,#1358);
#1073=LINE('',#5757,#1359);
#1074=LINE('',#5763,#1360);
#1075=LINE('',#5769,#1361);
#1076=LINE('',#5775,#1362);
#1077=LINE('',#5781,#1363);
#1078=LINE('',#5787,#1364);
#1079=LINE('',#5793,#1365);
#1080=LINE('',#5799,#1366);
#1081=LINE('',#5805,#1367);
#1341=VECTOR('',#4496,10.);
#1342=VECTOR('',#4499,10.);
#1343=VECTOR('',#4502,10.);
#1344=VECTOR('',#4503,10.);
#1345=VECTOR('',#4504,10.);
#1346=VECTOR('',#4507,10.);
#1347=VECTOR('',#4508,10.);
#1348=VECTOR('',#4509,10.);
#1349=VECTOR('',#4514,34.);
#1350=VECTOR('',#4523,35.);
#1351=VECTOR('',#4534,1.1);
#1352=VECTOR('',#4541,1.1);
#1353=VECTOR('',#4548,25.);
#1354=VECTOR('',#4555,1.1);
#1355=VECTOR('',#4562,1.1);
#1356=VECTOR('',#4569,1.1);
#1357=VECTOR('',#4576,1.1);
#1358=VECTOR('',#4583,1.1);
#1359=VECTOR('',#4590,1.1);
#1360=VECTOR('',#4597,1.1);
#1361=VECTOR('',#4604,1.1);
#1362=VECTOR('',#4611,1.1);
#1363=VECTOR('',#4618,1.1);
#1364=VECTOR('',#4625,1.1);
#1365=VECTOR('',#4632,1.1);
#1366=VECTOR('',#4639,1.1);
#1367=VECTOR('',#4646,1.1);
#1635=VERTEX_POINT('',#5670);
#1636=VERTEX_POINT('',#5671);
#1637=VERTEX_POINT('',#5673);
#1638=VERTEX_POINT('',#5675);
#1639=VERTEX_POINT('',#5679);
#1640=VERTEX_POINT('',#5681);
#1641=VERTEX_POINT('',#5685);
#1642=VERTEX_POINT('',#5687);
#1643=VERTEX_POINT('',#5691);
#1644=VERTEX_POINT('',#5693);
#1645=VERTEX_POINT('',#5698);
#1646=VERTEX_POINT('',#5700);
#1647=VERTEX_POINT('',#5706);
#1648=VERTEX_POINT('',#5708);
#1649=VERTEX_POINT('',#5712);
#1650=VERTEX_POINT('',#5714);
#1651=VERTEX_POINT('',#5718);
#1652=VERTEX_POINT('',#5720);
#1653=VERTEX_POINT('',#5724);
#1654=VERTEX_POINT('',#5726);
#1655=VERTEX_POINT('',#5730);
#1656=VERTEX_POINT('',#5732);
#1657=VERTEX_POINT('',#5736);
#1658=VERTEX_POINT('',#5738);
#1659=VERTEX_POINT('',#5742);
#1660=VERTEX_POINT('',#5744);
#1661=VERTEX_POINT('',#5748);
#1662=VERTEX_POINT('',#5750);
#1663=VERTEX_POINT('',#5754);
#1664=VERTEX_POINT('',#5756);
#1665=VERTEX_POINT('',#5760);
#1666=VERTEX_POINT('',#5762);
#1667=VERTEX_POINT('',#5766);
#1668=VERTEX_POINT('',#5768);
#1669=VERTEX_POINT('',#5772);
#1670=VERTEX_POINT('',#5774);
#1671=VERTEX_POINT('',#5778);
#1672=VERTEX_POINT('',#5780);
#1673=VERTEX_POINT('',#5784);
#1674=VERTEX_POINT('',#5786);
#1675=VERTEX_POINT('',#5790);
#1676=VERTEX_POINT('',#5792);
#1677=VERTEX_POINT('',#5796);
#1678=VERTEX_POINT('',#5798);
#1679=VERTEX_POINT('',#5802);
#1680=VERTEX_POINT('',#5804);
#1991=EDGE_CURVE('',#1635,#1636,#839,.T.);
#1992=EDGE_CURVE('',#1635,#1637,#1055,.T.);
#1993=EDGE_CURVE('',#1638,#1637,#840,.T.);
#1994=EDGE_CURVE('',#1636,#1638,#1056,.T.);
#1995=EDGE_CURVE('',#1636,#1639,#1057,.T.);
#1996=EDGE_CURVE('',#1640,#1638,#1058,.T.);
#1997=EDGE_CURVE('',#1639,#1640,#1059,.T.);
#1998=EDGE_CURVE('',#1641,#1635,#1060,.T.);
#1999=EDGE_CURVE('',#1641,#1642,#1061,.T.);
#2000=EDGE_CURVE('',#1637,#1642,#1062,.T.);
#2001=EDGE_CURVE('',#1643,#1643,#841,.T.);
#2002=EDGE_CURVE('',#1643,#1644,#1063,.T.);
#2003=EDGE_CURVE('',#1641,#1644,#842,.T.);
#2004=EDGE_CURVE('',#1644,#1639,#843,.T.);
#2005=EDGE_CURVE('',#1645,#1645,#844,.T.);
#2006=EDGE_CURVE('',#1645,#1646,#1064,.T.);
#2007=EDGE_CURVE('',#1646,#1646,#845,.T.);
#2008=EDGE_CURVE('',#1642,#1640,#846,.T.);
#2009=EDGE_CURVE('',#1647,#1647,#847,.T.);
#2010=EDGE_CURVE('',#1647,#1648,#1065,.T.);
#2011=EDGE_CURVE('',#1648,#1648,#848,.T.);
#2012=EDGE_CURVE('',#1649,#1649,#849,.T.);
#2013=EDGE_CURVE('',#1649,#1650,#1066,.T.);
#2014=EDGE_CURVE('',#1650,#1650,#850,.T.);
#2015=EDGE_CURVE('',#1651,#1651,#851,.T.);
#2016=EDGE_CURVE('',#1651,#1652,#1067,.T.);
#2017=EDGE_CURVE('',#1652,#1652,#852,.T.);
#2018=EDGE_CURVE('',#1653,#1653,#853,.T.);
#2019=EDGE_CURVE('',#1653,#1654,#1068,.T.);
#2020=EDGE_CURVE('',#1654,#1654,#854,.T.);
#2021=EDGE_CURVE('',#1655,#1655,#855,.T.);
#2022=EDGE_CURVE('',#1655,#1656,#1069,.T.);
#2023=EDGE_CURVE('',#1656,#1656,#856,.T.);
#2024=EDGE_CURVE('',#1657,#1657,#857,.T.);
#2025=EDGE_CURVE('',#1657,#1658,#1070,.T.);
#2026=EDGE_CURVE('',#1658,#1658,#858,.T.);
#2027=EDGE_CURVE('',#1659,#1659,#859,.T.);
#2028=EDGE_CURVE('',#1659,#1660,#1071,.T.);
#2029=EDGE_CURVE('',#1660,#1660,#860,.T.);
#2030=EDGE_CURVE('',#1661,#1661,#861,.T.);
#2031=EDGE_CURVE('',#1661,#1662,#1072,.T.);
#2032=EDGE_CURVE('',#1662,#1662,#862,.T.);
#2033=EDGE_CURVE('',#1663,#1663,#863,.T.);
#2034=EDGE_CURVE('',#1663,#1664,#1073,.T.);
#2035=EDGE_CURVE('',#1664,#1664,#864,.T.);
#2036=EDGE_CURVE('',#1665,#1665,#865,.T.);
#2037=EDGE_CURVE('',#1665,#1666,#1074,.T.);
#2038=EDGE_CURVE('',#1666,#1666,#866,.T.);
#2039=EDGE_CURVE('',#1667,#1667,#867,.T.);
#2040=EDGE_CURVE('',#1667,#1668,#1075,.T.);
#2041=EDGE_CURVE('',#1668,#1668,#868,.T.);
#2042=EDGE_CURVE('',#1669,#1669,#869,.T.);
#2043=EDGE_CURVE('',#1669,#1670,#1076,.T.);
#2044=EDGE_CURVE('',#1670,#1670,#870,.T.);
#2045=EDGE_CURVE('',#1671,#1671,#871,.T.);
#2046=EDGE_CURVE('',#1671,#1672,#1077,.T.);
#2047=EDGE_CURVE('',#1672,#1672,#872,.T.);
#2048=EDGE_CURVE('',#1673,#1673,#873,.T.);
#2049=EDGE_CURVE('',#1673,#1674,#1078,.T.);
#2050=EDGE_CURVE('',#1674,#1674,#874,.T.);
#2051=EDGE_CURVE('',#1675,#1675,#875,.T.);
#2052=EDGE_CURVE('',#1675,#1676,#1079,.T.);
#2053=EDGE_CURVE('',#1676,#1676,#876,.T.);
#2054=EDGE_CURVE('',#1677,#1677,#877,.T.);
#2055=EDGE_CURVE('',#1677,#1678,#1080,.T.);
#2056=EDGE_CURVE('',#1678,#1678,#878,.T.);
#2057=EDGE_CURVE('',#1679,#1679,#879,.T.);
#2058=EDGE_CURVE('',#1679,#1680,#1081,.T.);
#2059=EDGE_CURVE('',#1680,#1680,#880,.T.);
#2548=ORIENTED_EDGE('',*,*,#1991,.F.);
#2549=ORIENTED_EDGE('',*,*,#1992,.T.);
#2550=ORIENTED_EDGE('',*,*,#1993,.F.);
#2551=ORIENTED_EDGE('',*,*,#1994,.F.);
#2552=ORIENTED_EDGE('',*,*,#1995,.F.);
#2553=ORIENTED_EDGE('',*,*,#1994,.T.);
#2554=ORIENTED_EDGE('',*,*,#1996,.F.);
#2555=ORIENTED_EDGE('',*,*,#1997,.F.);
#2556=ORIENTED_EDGE('',*,*,#1998,.F.);
#2557=ORIENTED_EDGE('',*,*,#1999,.T.);
#2558=ORIENTED_EDGE('',*,*,#2000,.F.);
#2559=ORIENTED_EDGE('',*,*,#1992,.F.);
#2560=ORIENTED_EDGE('',*,*,#2001,.F.);
#2561=ORIENTED_EDGE('',*,*,#2002,.T.);
#2562=ORIENTED_EDGE('',*,*,#2003,.F.);
#2563=ORIENTED_EDGE('',*,*,#1998,.T.);
#2564=ORIENTED_EDGE('',*,*,#1991,.T.);
#2565=ORIENTED_EDGE('',*,*,#1995,.T.);
#2566=ORIENTED_EDGE('',*,*,#2004,.F.);
#2567=ORIENTED_EDGE('',*,*,#2002,.F.);
#2568=ORIENTED_EDGE('',*,*,#2005,.F.);
#2569=ORIENTED_EDGE('',*,*,#2006,.T.);
#2570=ORIENTED_EDGE('',*,*,#2007,.F.);
#2571=ORIENTED_EDGE('',*,*,#2006,.F.);
#2572=ORIENTED_EDGE('',*,*,#2008,.T.);
#2573=ORIENTED_EDGE('',*,*,#1996,.T.);
#2574=ORIENTED_EDGE('',*,*,#1993,.T.);
#2575=ORIENTED_EDGE('',*,*,#2000,.T.);
#2576=ORIENTED_EDGE('',*,*,#2005,.T.);
#2577=ORIENTED_EDGE('',*,*,#2001,.T.);
#2578=ORIENTED_EDGE('',*,*,#2009,.F.);
#2579=ORIENTED_EDGE('',*,*,#2010,.T.);
#2580=ORIENTED_EDGE('',*,*,#2011,.F.);
#2581=ORIENTED_EDGE('',*,*,#2010,.F.);
#2582=ORIENTED_EDGE('',*,*,#2012,.F.);
#2583=ORIENTED_EDGE('',*,*,#2013,.T.);
#2584=ORIENTED_EDGE('',*,*,#2014,.F.);
#2585=ORIENTED_EDGE('',*,*,#2013,.F.);
#2586=ORIENTED_EDGE('',*,*,#2015,.F.);
#2587=ORIENTED_EDGE('',*,*,#2016,.T.);
#2588=ORIENTED_EDGE('',*,*,#2017,.F.);
#2589=ORIENTED_EDGE('',*,*,#2016,.F.);
#2590=ORIENTED_EDGE('',*,*,#2018,.F.);
#2591=ORIENTED_EDGE('',*,*,#2019,.T.);
#2592=ORIENTED_EDGE('',*,*,#2020,.F.);
#2593=ORIENTED_EDGE('',*,*,#2019,.F.);
#2594=ORIENTED_EDGE('',*,*,#2021,.F.);
#2595=ORIENTED_EDGE('',*,*,#2022,.T.);
#2596=ORIENTED_EDGE('',*,*,#2023,.F.);
#2597=ORIENTED_EDGE('',*,*,#2022,.F.);
#2598=ORIENTED_EDGE('',*,*,#2024,.F.);
#2599=ORIENTED_EDGE('',*,*,#2025,.T.);
#2600=ORIENTED_EDGE('',*,*,#2026,.F.);
#2601=ORIENTED_EDGE('',*,*,#2025,.F.);
#2602=ORIENTED_EDGE('',*,*,#2027,.F.);
#2603=ORIENTED_EDGE('',*,*,#2028,.T.);
#2604=ORIENTED_EDGE('',*,*,#2029,.F.);
#2605=ORIENTED_EDGE('',*,*,#2028,.F.);
#2606=ORIENTED_EDGE('',*,*,#2030,.F.);
#2607=ORIENTED_EDGE('',*,*,#2031,.T.);
#2608=ORIENTED_EDGE('',*,*,#2032,.F.);
#2609=ORIENTED_EDGE('',*,*,#2031,.F.);
#2610=ORIENTED_EDGE('',*,*,#2033,.F.);
#2611=ORIENTED_EDGE('',*,*,#2034,.T.);
#2612=ORIENTED_EDGE('',*,*,#2035,.F.);
#2613=ORIENTED_EDGE('',*,*,#2034,.F.);
#2614=ORIENTED_EDGE('',*,*,#2036,.F.);
#2615=ORIENTED_EDGE('',*,*,#2037,.T.);
#2616=ORIENTED_EDGE('',*,*,#2038,.F.);
#2617=ORIENTED_EDGE('',*,*,#2037,.F.);
#2618=ORIENTED_EDGE('',*,*,#2039,.F.);
#2619=ORIENTED_EDGE('',*,*,#2040,.T.);
#2620=ORIENTED_EDGE('',*,*,#2041,.F.);
#2621=ORIENTED_EDGE('',*,*,#2040,.F.);
#2622=ORIENTED_EDGE('',*,*,#2042,.F.);
#2623=ORIENTED_EDGE('',*,*,#2043,.T.);
#2624=ORIENTED_EDGE('',*,*,#2044,.F.);
#2625=ORIENTED_EDGE('',*,*,#2043,.F.);
#2626=ORIENTED_EDGE('',*,*,#2045,.F.);
#2627=ORIENTED_EDGE('',*,*,#2046,.T.);
#2628=ORIENTED_EDGE('',*,*,#2047,.F.);
#2629=ORIENTED_EDGE('',*,*,#2046,.F.);
#2630=ORIENTED_EDGE('',*,*,#2048,.F.);
#2631=ORIENTED_EDGE('',*,*,#2049,.T.);
#2632=ORIENTED_EDGE('',*,*,#2050,.F.);
#2633=ORIENTED_EDGE('',*,*,#2049,.F.);
#2634=ORIENTED_EDGE('',*,*,#2051,.F.);
#2635=ORIENTED_EDGE('',*,*,#2052,.T.);
#2636=ORIENTED_EDGE('',*,*,#2053,.F.);
#2637=ORIENTED_EDGE('',*,*,#2052,.F.);
#2638=ORIENTED_EDGE('',*,*,#2054,.F.);
#2639=ORIENTED_EDGE('',*,*,#2055,.T.);
#2640=ORIENTED_EDGE('',*,*,#2056,.F.);
#2641=ORIENTED_EDGE('',*,*,#2055,.F.);
#2642=ORIENTED_EDGE('',*,*,#2057,.F.);
#2643=ORIENTED_EDGE('',*,*,#2058,.T.);
#2644=ORIENTED_EDGE('',*,*,#2059,.F.);
#2645=ORIENTED_EDGE('',*,*,#2058,.F.);
#2646=ORIENTED_EDGE('',*,*,#2007,.T.);
#2647=ORIENTED_EDGE('',*,*,#2059,.T.);
#2648=ORIENTED_EDGE('',*,*,#2056,.T.);
#2649=ORIENTED_EDGE('',*,*,#2053,.T.);
#2650=ORIENTED_EDGE('',*,*,#2050,.T.);
#2651=ORIENTED_EDGE('',*,*,#2047,.T.);
#2652=ORIENTED_EDGE('',*,*,#2044,.T.);
#2653=ORIENTED_EDGE('',*,*,#2041,.T.);
#2654=ORIENTED_EDGE('',*,*,#2038,.T.);
#2655=ORIENTED_EDGE('',*,*,#2035,.T.);
#2656=ORIENTED_EDGE('',*,*,#2032,.T.);
#2657=ORIENTED_EDGE('',*,*,#2029,.T.);
#2658=ORIENTED_EDGE('',*,*,#2026,.T.);
#2659=ORIENTED_EDGE('',*,*,#2023,.T.);
#2660=ORIENTED_EDGE('',*,*,#2020,.T.);
#2661=ORIENTED_EDGE('',*,*,#2017,.T.);
#2662=ORIENTED_EDGE('',*,*,#2014,.T.);
#2663=ORIENTED_EDGE('',*,*,#2011,.T.);
#2664=ORIENTED_EDGE('',*,*,#2003,.T.);
#2665=ORIENTED_EDGE('',*,*,#2004,.T.);
#2666=ORIENTED_EDGE('',*,*,#1997,.T.);
#2667=ORIENTED_EDGE('',*,*,#2008,.F.);
#2668=ORIENTED_EDGE('',*,*,#1999,.F.);
#2669=ORIENTED_EDGE('',*,*,#2015,.T.);
#2670=ORIENTED_EDGE('',*,*,#2030,.T.);
#2671=ORIENTED_EDGE('',*,*,#2042,.T.);
#2672=ORIENTED_EDGE('',*,*,#2057,.T.);
#2673=ORIENTED_EDGE('',*,*,#2033,.T.);
#2674=ORIENTED_EDGE('',*,*,#2027,.T.);
#2675=ORIENTED_EDGE('',*,*,#2024,.T.);
#2676=ORIENTED_EDGE('',*,*,#2021,.T.);
#2677=ORIENTED_EDGE('',*,*,#2018,.T.);
#2678=ORIENTED_EDGE('',*,*,#2009,.T.);
#2679=ORIENTED_EDGE('',*,*,#2012,.T.);
#2680=ORIENTED_EDGE('',*,*,#2036,.T.);
#2681=ORIENTED_EDGE('',*,*,#2039,.T.);
#2682=ORIENTED_EDGE('',*,*,#2045,.T.);
#2683=ORIENTED_EDGE('',*,*,#2048,.T.);
#2684=ORIENTED_EDGE('',*,*,#2051,.T.);
#2685=ORIENTED_EDGE('',*,*,#2054,.T.);
#3487=CYLINDRICAL_SURFACE('',#3966,34.);
#3488=CYLINDRICAL_SURFACE('',#3970,35.);
#3489=CYLINDRICAL_SURFACE('',#3975,1.1);
#3490=CYLINDRICAL_SURFACE('',#3978,1.1);
#3491=CYLINDRICAL_SURFACE('',#3981,25.);
#3492=CYLINDRICAL_SURFACE('',#3984,1.1);
#3493=CYLINDRICAL_SURFACE('',#3987,1.1);
#3494=CYLINDRICAL_SURFACE('',#3990,1.1);
#3495=CYLINDRICAL_SURFACE('',#3993,1.1);
#3496=CYLINDRICAL_SURFACE('',#3996,1.1);
#3497=CYLINDRICAL_SURFACE('',#3999,1.1);
#3498=CYLINDRICAL_SURFACE('',#4002,1.1);
#3499=CYLINDRICAL_SURFACE('',#4005,1.1);
#3500=CYLINDRICAL_SURFACE('',#4008,1.1);
#3501=CYLINDRICAL_SURFACE('',#4011,1.1);
#3502=CYLINDRICAL_SURFACE('',#4014,1.1);
#3503=CYLINDRICAL_SURFACE('',#4017,1.1);
#3504=CYLINDRICAL_SURFACE('',#4020,1.1);
#3505=CYLINDRICAL_SURFACE('',#4023,1.1);
#3563=ADVANCED_FACE('',(#357),#200,.F.);
#3564=ADVANCED_FACE('',(#358),#201,.F.);
#3565=ADVANCED_FACE('',(#359),#202,.F.);
#3566=ADVANCED_FACE('',(#360),#3487,.F.);
#3567=ADVANCED_FACE('',(#361,#134),#3488,.T.);
#3568=ADVANCED_FACE('',(#362,#135),#203,.F.);
#3569=ADVANCED_FACE('',(#363),#3489,.F.);
#3570=ADVANCED_FACE('',(#364),#3490,.F.);
#3571=ADVANCED_FACE('',(#365),#3491,.F.);
#3572=ADVANCED_FACE('',(#366),#3492,.F.);
#3573=ADVANCED_FACE('',(#367),#3493,.F.);
#3574=ADVANCED_FACE('',(#368),#3494,.F.);
#3575=ADVANCED_FACE('',(#369),#3495,.F.);
#3576=ADVANCED_FACE('',(#370),#3496,.F.);
#3577=ADVANCED_FACE('',(#371),#3497,.F.);
#3578=ADVANCED_FACE('',(#372),#3498,.F.);
#3579=ADVANCED_FACE('',(#373),#3499,.F.);
#3580=ADVANCED_FACE('',(#374),#3500,.F.);
#3581=ADVANCED_FACE('',(#375),#3501,.F.);
#3582=ADVANCED_FACE('',(#376),#3502,.F.);
#3583=ADVANCED_FACE('',(#377),#3503,.F.);
#3584=ADVANCED_FACE('',(#378),#3504,.F.);
#3585=ADVANCED_FACE('',(#379),#3505,.F.);
#3586=ADVANCED_FACE('',(#380,#136,#137,#138,#139,#140,#141,#142,#143,#144,
#145,#146,#147,#148,#149,#150,#151,#152),#204,.T.);
#3587=ADVANCED_FACE('',(#381,#153,#154,#155,#156,#157,#158,#159,#160,#161,
#162,#163,#164,#165,#166,#167,#168,#169),#205,.F.);
#3755=CLOSED_SHELL('',(#3563,#3564,#3565,#3566,#3567,#3568,#3569,#3570,
#3571,#3572,#3573,#3574,#3575,#3576,#3577,#3578,#3579,#3580,#3581,#3582,
#3583,#3584,#3585,#3586,#3587));
#3960=AXIS2_PLACEMENT_3D('',#5668,#4490,#4491);
#3961=AXIS2_PLACEMENT_3D('',#5669,#4492,#4493);
#3962=AXIS2_PLACEMENT_3D('',#5672,#4494,#4495);
#3963=AXIS2_PLACEMENT_3D('',#5676,#4497,#4498);
#3964=AXIS2_PLACEMENT_3D('',#5678,#4500,#4501);
#3965=AXIS2_PLACEMENT_3D('',#5684,#4505,#4506);
#3966=AXIS2_PLACEMENT_3D('',#5690,#4510,#4511);
#3967=AXIS2_PLACEMENT_3D('',#5692,#4512,#4513);
#3968=AXIS2_PLACEMENT_3D('',#5695,#4515,#4516);
#3969=AXIS2_PLACEMENT_3D('',#5696,#4517,#4518);
#3970=AXIS2_PLACEMENT_3D('',#5697,#4519,#4520);
#3971=AXIS2_PLACEMENT_3D('',#5699,#4521,#4522);
#3972=AXIS2_PLACEMENT_3D('',#5702,#4524,#4525);
#3973=AXIS2_PLACEMENT_3D('',#5703,#4526,#4527);
#3974=AXIS2_PLACEMENT_3D('',#5704,#4528,#4529);
#3975=AXIS2_PLACEMENT_3D('',#5705,#4530,#4531);
#3976=AXIS2_PLACEMENT_3D('',#5707,#4532,#4533);
#3977=AXIS2_PLACEMENT_3D('',#5710,#4535,#4536);
#3978=AXIS2_PLACEMENT_3D('',#5711,#4537,#4538);
#3979=AXIS2_PLACEMENT_3D('',#5713,#4539,#4540);
#3980=AXIS2_PLACEMENT_3D('',#5716,#4542,#4543);
#3981=AXIS2_PLACEMENT_3D('',#5717,#4544,#4545);
#3982=AXIS2_PLACEMENT_3D('',#5719,#4546,#4547);
#3983=AXIS2_PLACEMENT_3D('',#5722,#4549,#4550);
#3984=AXIS2_PLACEMENT_3D('',#5723,#4551,#4552);
#3985=AXIS2_PLACEMENT_3D('',#5725,#4553,#4554);
#3986=AXIS2_PLACEMENT_3D('',#5728,#4556,#4557);
#3987=AXIS2_PLACEMENT_3D('',#5729,#4558,#4559);
#3988=AXIS2_PLACEMENT_3D('',#5731,#4560,#4561);
#3989=AXIS2_PLACEMENT_3D('',#5734,#4563,#4564);
#3990=AXIS2_PLACEMENT_3D('',#5735,#4565,#4566);
#3991=AXIS2_PLACEMENT_3D('',#5737,#4567,#4568);
#3992=AXIS2_PLACEMENT_3D('',#5740,#4570,#4571);
#3993=AXIS2_PLACEMENT_3D('',#5741,#4572,#4573);
#3994=AXIS2_PLACEMENT_3D('',#5743,#4574,#4575);
#3995=AXIS2_PLACEMENT_3D('',#5746,#4577,#4578);
#3996=AXIS2_PLACEMENT_3D('',#5747,#4579,#4580);
#3997=AXIS2_PLACEMENT_3D('',#5749,#4581,#4582);
#3998=AXIS2_PLACEMENT_3D('',#5752,#4584,#4585);
#3999=AXIS2_PLACEMENT_3D('',#5753,#4586,#4587);
#4000=AXIS2_PLACEMENT_3D('',#5755,#4588,#4589);
#4001=AXIS2_PLACEMENT_3D('',#5758,#4591,#4592);
#4002=AXIS2_PLACEMENT_3D('',#5759,#4593,#4594);
#4003=AXIS2_PLACEMENT_3D('',#5761,#4595,#4596);
#4004=AXIS2_PLACEMENT_3D('',#5764,#4598,#4599);
#4005=AXIS2_PLACEMENT_3D('',#5765,#4600,#4601);
#4006=AXIS2_PLACEMENT_3D('',#5767,#4602,#4603);
#4007=AXIS2_PLACEMENT_3D('',#5770,#4605,#4606);
#4008=AXIS2_PLACEMENT_3D('',#5771,#4607,#4608);
#4009=AXIS2_PLACEMENT_3D('',#5773,#4609,#4610);
#4010=AXIS2_PLACEMENT_3D('',#5776,#4612,#4613);
#4011=AXIS2_PLACEMENT_3D('',#5777,#4614,#4615);
#4012=AXIS2_PLACEMENT_3D('',#5779,#4616,#4617);
#4013=AXIS2_PLACEMENT_3D('',#5782,#4619,#4620);
#4014=AXIS2_PLACEMENT_3D('',#5783,#4621,#4622);
#4015=AXIS2_PLACEMENT_3D('',#5785,#4623,#4624);
#4016=AXIS2_PLACEMENT_3D('',#5788,#4626,#4627);
#4017=AXIS2_PLACEMENT_3D('',#5789,#4628,#4629);
#4018=AXIS2_PLACEMENT_3D('',#5791,#4630,#4631);
#4019=AXIS2_PLACEMENT_3D('',#5794,#4633,#4634);
#4020=AXIS2_PLACEMENT_3D('',#5795,#4635,#4636);
#4021=AXIS2_PLACEMENT_3D('',#5797,#4637,#4638);
#4022=AXIS2_PLACEMENT_3D('',#5800,#4640,#4641);
#4023=AXIS2_PLACEMENT_3D('',#5801,#4642,#4643);
#4024=AXIS2_PLACEMENT_3D('',#5803,#4644,#4645);
#4025=AXIS2_PLACEMENT_3D('',#5806,#4647,#4648);
#4026=AXIS2_PLACEMENT_3D('',#5807,#4649,#4650);
#4027=AXIS2_PLACEMENT_3D('',#5808,#4651,#4652);
#4490=DIRECTION('axis',(0.,0.,1.));
#4491=DIRECTION('refdir',(1.,0.,0.));
#4492=DIRECTION('center_axis',(0.,1.,0.));
#4493=DIRECTION('ref_axis',(-1.,0.,0.));
#4494=DIRECTION('center_axis',(0.,-1.,0.));
#4495=DIRECTION('ref_axis',(1.,0.,0.));
#4496=DIRECTION('',(0.,0.,1.));
#4497=DIRECTION('center_axis',(0.,1.,0.));
#4498=DIRECTION('ref_axis',(1.,0.,0.));
#4499=DIRECTION('',(0.,0.,1.));
#4500=DIRECTION('center_axis',(-1.,0.,0.));
#4501=DIRECTION('ref_axis',(0.,-1.,0.));
#4502=DIRECTION('',(0.,-1.,0.));
#4503=DIRECTION('',(0.,1.,0.));
#4504=DIRECTION('',(0.,0.,1.));
#4505=DIRECTION('center_axis',(1.,0.,0.));
#4506=DIRECTION('ref_axis',(0.,1.,0.));
#4507=DIRECTION('',(0.,1.,0.));
#4508=DIRECTION('',(0.,0.,1.));
#4509=DIRECTION('',(0.,-1.,0.));
#4510=DIRECTION('center_axis',(0.,1.,0.));
#4511=DIRECTION('ref_axis',(1.,0.,0.));
#4512=DIRECTION('center_axis',(0.,-1.,0.));
#4513=DIRECTION('ref_axis',(1.,0.,0.));
#4514=DIRECTION('',(0.,-1.,0.));
#4515=DIRECTION('center_axis',(0.,1.,0.));
#4516=DIRECTION('ref_axis',(1.,0.,0.));
#4517=DIRECTION('center_axis',(0.,1.,0.));
#4518=DIRECTION('ref_axis',(1.,0.,0.));
#4519=DIRECTION('center_axis',(0.,1.,0.));
#4520=DIRECTION('ref_axis',(1.,0.,0.));
#4521=DIRECTION('center_axis',(0.,1.,0.));
#4522=DIRECTION('ref_axis',(1.,0.,0.));
#4523=DIRECTION('',(0.,-1.,0.));
#4524=DIRECTION('center_axis',(0.,-1.,0.));
#4525=DIRECTION('ref_axis',(1.,0.,0.));
#4526=DIRECTION('center_axis',(0.,-1.,0.));
#4527=DIRECTION('ref_axis',(1.,0.,0.));
#4528=DIRECTION('center_axis',(0.,-1.,0.));
#4529=DIRECTION('ref_axis',(1.,0.,0.));
#4530=DIRECTION('center_axis',(0.,1.,0.));
#4531=DIRECTION('ref_axis',(1.,0.,0.));
#4532=DIRECTION('center_axis',(0.,-1.,0.));
#4533=DIRECTION('ref_axis',(1.,0.,0.));
#4534=DIRECTION('',(0.,-1.,0.));
#4535=DIRECTION('center_axis',(0.,1.,0.));
#4536=DIRECTION('ref_axis',(1.,0.,0.));
#4537=DIRECTION('center_axis',(0.,1.,0.));
#4538=DIRECTION('ref_axis',(1.,0.,0.));
#4539=DIRECTION('center_axis',(0.,-1.,0.));
#4540=DIRECTION('ref_axis',(1.,0.,0.));
#4541=DIRECTION('',(0.,-1.,0.));
#4542=DIRECTION('center_axis',(0.,1.,0.));
#4543=DIRECTION('ref_axis',(1.,0.,0.));
#4544=DIRECTION('center_axis',(0.,1.,0.));
#4545=DIRECTION('ref_axis',(1.,0.,0.));
#4546=DIRECTION('center_axis',(0.,-1.,0.));
#4547=DIRECTION('ref_axis',(1.,0.,0.));
#4548=DIRECTION('',(0.,-1.,0.));
#4549=DIRECTION('center_axis',(0.,1.,0.));
#4550=DIRECTION('ref_axis',(1.,0.,0.));
#4551=DIRECTION('center_axis',(0.,1.,0.));
#4552=DIRECTION('ref_axis',(1.,0.,0.));
#4553=DIRECTION('center_axis',(0.,-1.,0.));
#4554=DIRECTION('ref_axis',(1.,0.,0.));
#4555=DIRECTION('',(0.,-1.,0.));
#4556=DIRECTION('center_axis',(0.,1.,0.));
#4557=DIRECTION('ref_axis',(1.,0.,0.));
#4558=DIRECTION('center_axis',(0.,1.,0.));
#4559=DIRECTION('ref_axis',(1.,0.,0.));
#4560=DIRECTION('center_axis',(0.,-1.,0.));
#4561=DIRECTION('ref_axis',(1.,0.,0.));
#4562=DIRECTION('',(0.,-1.,0.));
#4563=DIRECTION('center_axis',(0.,1.,0.));
#4564=DIRECTION('ref_axis',(1.,0.,0.));
#4565=DIRECTION('center_axis',(0.,1.,0.));
#4566=DIRECTION('ref_axis',(1.,0.,0.));
#4567=DIRECTION('center_axis',(0.,-1.,0.));
#4568=DIRECTION('ref_axis',(1.,0.,0.));
#4569=DIRECTION('',(0.,-1.,0.));
#4570=DIRECTION('center_axis',(0.,1.,0.));
#4571=DIRECTION('ref_axis',(1.,0.,0.));
#4572=DIRECTION('center_axis',(0.,1.,0.));
#4573=DIRECTION('ref_axis',(1.,0.,0.));
#4574=DIRECTION('center_axis',(0.,-1.,0.));
#4575=DIRECTION('ref_axis',(1.,0.,0.));
#4576=DIRECTION('',(0.,-1.,0.));
#4577=DIRECTION('center_axis',(0.,1.,0.));
#4578=DIRECTION('ref_axis',(1.,0.,0.));
#4579=DIRECTION('center_axis',(0.,1.,0.));
#4580=DIRECTION('ref_axis',(1.,0.,0.));
#4581=DIRECTION('center_axis',(0.,-1.,0.));
#4582=DIRECTION('ref_axis',(1.,0.,0.));
#4583=DIRECTION('',(0.,-1.,0.));
#4584=DIRECTION('center_axis',(0.,1.,0.));
#4585=DIRECTION('ref_axis',(1.,0.,0.));
#4586=DIRECTION('center_axis',(0.,1.,0.));
#4587=DIRECTION('ref_axis',(1.,0.,0.));
#4588=DIRECTION('center_axis',(0.,-1.,0.));
#4589=DIRECTION('ref_axis',(1.,0.,0.));
#4590=DIRECTION('',(0.,-1.,0.));
#4591=DIRECTION('center_axis',(0.,1.,0.));
#4592=DIRECTION('ref_axis',(1.,0.,0.));
#4593=DIRECTION('center_axis',(0.,1.,0.));
#4594=DIRECTION('ref_axis',(1.,0.,0.));
#4595=DIRECTION('center_axis',(0.,-1.,0.));
#4596=DIRECTION('ref_axis',(1.,0.,0.));
#4597=DIRECTION('',(0.,-1.,0.));
#4598=DIRECTION('center_axis',(0.,1.,0.));
#4599=DIRECTION('ref_axis',(1.,0.,0.));
#4600=DIRECTION('center_axis',(0.,1.,0.));
#4601=DIRECTION('ref_axis',(1.,0.,0.));
#4602=DIRECTION('center_axis',(0.,-1.,0.));
#4603=DIRECTION('ref_axis',(1.,0.,0.));
#4604=DIRECTION('',(0.,-1.,0.));
#4605=DIRECTION('center_axis',(0.,1.,0.));
#4606=DIRECTION('ref_axis',(1.,0.,0.));
#4607=DIRECTION('center_axis',(0.,1.,0.));
#4608=DIRECTION('ref_axis',(1.,0.,0.));
#4609=DIRECTION('center_axis',(0.,-1.,0.));
#4610=DIRECTION('ref_axis',(1.,0.,0.));
#4611=DIRECTION('',(0.,-1.,0.));
#4612=DIRECTION('center_axis',(0.,1.,0.));
#4613=DIRECTION('ref_axis',(1.,0.,0.));
#4614=DIRECTION('center_axis',(0.,1.,0.));
#4615=DIRECTION('ref_axis',(1.,0.,0.));
#4616=DIRECTION('center_axis',(0.,-1.,0.));
#4617=DIRECTION('ref_axis',(1.,0.,0.));
#4618=DIRECTION('',(0.,-1.,0.));
#4619=DIRECTION('center_axis',(0.,1.,0.));
#4620=DIRECTION('ref_axis',(1.,0.,0.));
#4621=DIRECTION('center_axis',(0.,1.,0.));
#4622=DIRECTION('ref_axis',(1.,0.,0.));
#4623=DIRECTION('center_axis',(0.,-1.,0.));
#4624=DIRECTION('ref_axis',(1.,0.,0.));
#4625=DIRECTION('',(0.,-1.,0.));
#4626=DIRECTION('center_axis',(0.,1.,0.));
#4627=DIRECTION('ref_axis',(1.,0.,0.));
#4628=DIRECTION('center_axis',(0.,1.,0.));
#4629=DIRECTION('ref_axis',(1.,0.,0.));
#4630=DIRECTION('center_axis',(0.,-1.,0.));
#4631=DIRECTION('ref_axis',(1.,0.,0.));
#4632=DIRECTION('',(0.,-1.,0.));
#4633=DIRECTION('center_axis',(0.,1.,0.));
#4634=DIRECTION('ref_axis',(1.,0.,0.));
#4635=DIRECTION('center_axis',(0.,1.,0.));
#4636=DIRECTION('ref_axis',(1.,0.,0.));
#4637=DIRECTION('center_axis',(0.,-1.,0.));
#4638=DIRECTION('ref_axis',(1.,0.,0.));
#4639=DIRECTION('',(0.,-1.,0.));
#4640=DIRECTION('center_axis',(0.,1.,0.));
#4641=DIRECTION('ref_axis',(1.,0.,0.));
#4642=DIRECTION('center_axis',(0.,1.,0.));
#4643=DIRECTION('ref_axis',(1.,0.,0.));
#4644=DIRECTION('center_axis',(0.,-1.,0.));
#4645=DIRECTION('ref_axis',(1.,0.,0.));
#4646=DIRECTION('',(0.,-1.,0.));
#4647=DIRECTION('center_axis',(0.,1.,0.));
#4648=DIRECTION('ref_axis',(1.,0.,0.));
#4649=DIRECTION('center_axis',(0.,-1.,0.));
#4650=DIRECTION('ref_axis',(1.,0.,0.));
#4651=DIRECTION('center_axis',(0.,-1.,0.));
#4652=DIRECTION('ref_axis',(1.,0.,0.));
#5668=CARTESIAN_POINT('',(0.,0.,0.));
#5669=CARTESIAN_POINT('Origin',(27.848517275114,2.,0.));
#5670=CARTESIAN_POINT('',(27.848517275114,2.,133.837794222876));
#5671=CARTESIAN_POINT('',(-27.848517275114,2.,133.837794222876));
#5672=CARTESIAN_POINT('Origin',(-2.22044604925031E-15,2.,114.33240815703));
#5673=CARTESIAN_POINT('',(27.848517275114,2.,135.532881868193));
#5674=CARTESIAN_POINT('',(27.848517275114,2.,0.));
#5675=CARTESIAN_POINT('',(-27.848517275114,2.,135.532881868193));
#5676=CARTESIAN_POINT('Origin',(-2.22044604925031E-15,2.,114.33240815703));
#5677=CARTESIAN_POINT('',(-27.848517275114,2.,0.));
#5678=CARTESIAN_POINT('Origin',(-27.848517275114,2.,0.));
#5679=CARTESIAN_POINT('',(-27.848517275114,-3.,133.837794222876));
#5680=CARTESIAN_POINT('',(-27.848517275114,-4.,133.837794222876));
#5681=CARTESIAN_POINT('',(-27.848517275114,-3.,135.532881868193));
#5682=CARTESIAN_POINT('',(-27.848517275114,-4.,135.532881868193));
#5683=CARTESIAN_POINT('',(-27.848517275114,-3.,0.));
#5684=CARTESIAN_POINT('Origin',(27.848517275114,-3.,0.));
#5685=CARTESIAN_POINT('',(27.848517275114,-3.,133.837794222876));
#5686=CARTESIAN_POINT('',(27.848517275114,-4.,133.837794222876));
#5687=CARTESIAN_POINT('',(27.848517275114,-3.,135.532881868193));
#5688=CARTESIAN_POINT('',(27.848517275114,-3.,0.));
#5689=CARTESIAN_POINT('',(27.848517275114,-4.,135.532881868193));
#5690=CARTESIAN_POINT('Origin',(-2.22044604925031E-15,-4.,114.33240815703));
#5691=CARTESIAN_POINT('',(-34.,3.,114.33240815703));
#5692=CARTESIAN_POINT('Origin',(-2.22044604925031E-15,3.,114.33240815703));
#5693=CARTESIAN_POINT('',(-34.,-3.,114.33240815703));
#5694=CARTESIAN_POINT('',(-34.,-4.,114.33240815703));
#5695=CARTESIAN_POINT('Origin',(-2.22044604925031E-15,-3.,114.33240815703));
#5696=CARTESIAN_POINT('Origin',(-2.22044604925031E-15,-3.,114.33240815703));
#5697=CARTESIAN_POINT('Origin',(-2.22044604925031E-15,-4.,114.33240815703));
#5698=CARTESIAN_POINT('',(-35.,3.,114.33240815703));
#5699=CARTESIAN_POINT('Origin',(-2.22044604925031E-15,3.,114.33240815703));
#5700=CARTESIAN_POINT('',(-35.,-4.,114.33240815703));
#5701=CARTESIAN_POINT('',(-35.,-4.,114.33240815703));
#5702=CARTESIAN_POINT('Origin',(-2.22044604925031E-15,-4.,114.33240815703));
#5703=CARTESIAN_POINT('Origin',(-2.22044604925031E-15,-3.,114.33240815703));
#5704=CARTESIAN_POINT('Origin',(0.,3.,114.33240815703));
#5705=CARTESIAN_POINT('Origin',(-16.7482292407074,-4.,90.3728422287138));
#5706=CARTESIAN_POINT('',(-17.8482292407074,-3.,90.3728422287138));
#5707=CARTESIAN_POINT('Origin',(-16.7482292407074,-3.,90.3728422287138));
#5708=CARTESIAN_POINT('',(-17.8482292407074,-4.,90.3728422287138));
#5709=CARTESIAN_POINT('',(-17.8482292407074,-4.,90.3728422287138));
#5710=CARTESIAN_POINT('Origin',(-16.7482292407074,-4.,90.3728422287138));
#5711=CARTESIAN_POINT('Origin',(-6.30441727387072,-4.,85.7873857361326));
#5712=CARTESIAN_POINT('',(-7.40441727387072,-3.,85.7873857361326));
#5713=CARTESIAN_POINT('Origin',(-6.30441727387072,-3.,85.7873857361326));
#5714=CARTESIAN_POINT('',(-7.40441727387072,-4.,85.7873857361326));
#5715=CARTESIAN_POINT('',(-7.40441727387072,-4.,85.7873857361326));
#5716=CARTESIAN_POINT('Origin',(-6.30441727387072,-4.,85.7873857361326));
#5717=CARTESIAN_POINT('Origin',(-2.22044604925031E-15,-4.,114.33240815703));
#5718=CARTESIAN_POINT('',(-25.,-3.,114.33240815703));
#5719=CARTESIAN_POINT('Origin',(-2.22044604925031E-15,-3.,114.33240815703));
#5720=CARTESIAN_POINT('',(-25.,-4.,114.33240815703));
#5721=CARTESIAN_POINT('',(-25.,-4.,114.33240815703));
#5722=CARTESIAN_POINT('Origin',(-2.22044604925031E-15,-4.,114.33240815703));
#5723=CARTESIAN_POINT('Origin',(24.6422751287225,-4.,130.058890874186));
#5724=CARTESIAN_POINT('',(23.5422751287225,-3.,130.058890874186));
#5725=CARTESIAN_POINT('Origin',(24.6422751287225,-3.,130.058890874186));
#5726=CARTESIAN_POINT('',(23.5422751287225,-4.,130.058890874186));
#5727=CARTESIAN_POINT('',(23.5422751287225,-4.,130.058890874186));
#5728=CARTESIAN_POINT('Origin',(24.6422751287225,-4.,130.058890874186));
#5729=CARTESIAN_POINT('Origin',(6.30441727387071,-4.,142.877430577928));
#5730=CARTESIAN_POINT('',(5.20441727387071,-3.,142.877430577928));
#5731=CARTESIAN_POINT('Origin',(6.30441727387071,-3.,142.877430577928));
#5732=CARTESIAN_POINT('',(5.20441727387071,-4.,142.877430577928));
#5733=CARTESIAN_POINT('',(5.20441727387071,-4.,142.877430577928));
#5734=CARTESIAN_POINT('Origin',(6.30441727387071,-4.,142.877430577928));
#5735=CARTESIAN_POINT('Origin',(-15.7264827171553,-4.,138.974683285753));
#5736=CARTESIAN_POINT('',(-16.8264827171553,-3.,138.974683285753));
#5737=CARTESIAN_POINT('Origin',(-15.7264827171553,-3.,138.974683285753));
#5738=CARTESIAN_POINT('',(-16.8264827171553,-4.,138.974683285753));
#5739=CARTESIAN_POINT('',(-16.8264827171553,-4.,138.974683285753));
#5740=CARTESIAN_POINT('Origin',(-15.7264827171553,-4.,138.974683285753));
#5741=CARTESIAN_POINT('Origin',(16.7482292407074,-4.,138.291974085347));
#5742=CARTESIAN_POINT('',(15.6482292407074,-3.,138.291974085347));
#5743=CARTESIAN_POINT('Origin',(16.7482292407074,-3.,138.291974085347));
#5744=CARTESIAN_POINT('',(15.6482292407074,-4.,138.291974085347));
#5745=CARTESIAN_POINT('',(15.6482292407074,-4.,138.291974085347));
#5746=CARTESIAN_POINT('Origin',(16.7482292407074,-4.,138.291974085347));
#5747=CARTESIAN_POINT('Origin',(28.7847580111699,-4.,119.431593230258));
#5748=CARTESIAN_POINT('',(27.6847580111699,-3.,119.431593230258));
#5749=CARTESIAN_POINT('Origin',(28.7847580111699,-3.,119.431593230258));
#5750=CARTESIAN_POINT('',(27.6847580111699,-4.,119.431593230258));
#5751=CARTESIAN_POINT('',(27.6847580111699,-4.,119.431593230258));
#5752=CARTESIAN_POINT('Origin',(28.7847580111699,-4.,119.431593230258));
#5753=CARTESIAN_POINT('Origin',(-23.9595659283167,-4.,131.080637397738));
#5754=CARTESIAN_POINT('',(-25.0595659283167,-3.,131.080637397738));
#5755=CARTESIAN_POINT('Origin',(-23.9595659283167,-3.,131.080637397738));
#5756=CARTESIAN_POINT('',(-25.0595659283167,-4.,131.080637397738));
#5757=CARTESIAN_POINT('',(-25.0595659283167,-4.,131.080637397738));
#5758=CARTESIAN_POINT('Origin',(-23.9595659283167,-4.,131.080637397738));
#5759=CARTESIAN_POINT('Origin',(15.7264827171553,-4.,89.6901330283079));
#5760=CARTESIAN_POINT('',(14.6264827171553,-3.,89.6901330283079));
#5761=CARTESIAN_POINT('Origin',(15.7264827171553,-3.,89.6901330283079));
#5762=CARTESIAN_POINT('',(14.6264827171553,-4.,89.6901330283079));
#5763=CARTESIAN_POINT('',(14.6264827171553,-4.,89.6901330283079));
#5764=CARTESIAN_POINT('Origin',(15.7264827171553,-4.,89.6901330283079));
#5765=CARTESIAN_POINT('Origin',(5.09918507322788,-4.,85.5476501458605));
#5766=CARTESIAN_POINT('',(3.99918507322788,-3.,85.5476501458605));
#5767=CARTESIAN_POINT('Origin',(5.09918507322788,-3.,85.5476501458605));
#5768=CARTESIAN_POINT('',(3.99918507322788,-4.,85.5476501458605));
#5769=CARTESIAN_POINT('',(3.99918507322788,-4.,85.5476501458605));
#5770=CARTESIAN_POINT('Origin',(5.09918507322788,-4.,85.5476501458605));
#5771=CARTESIAN_POINT('Origin',(-28.5450224208979,-4.,120.636825430901));
#5772=CARTESIAN_POINT('',(-29.6450224208979,-3.,120.636825430901));
#5773=CARTESIAN_POINT('Origin',(-28.5450224208979,-3.,120.636825430901));
#5774=CARTESIAN_POINT('',(-29.6450224208979,-4.,120.636825430901));
#5775=CARTESIAN_POINT('',(-29.6450224208979,-4.,120.636825430901));
#5776=CARTESIAN_POINT('Origin',(-28.5450224208979,-4.,120.636825430901));
#5777=CARTESIAN_POINT('Origin',(-24.6422751287225,-4.,98.6059254398751));
#5778=CARTESIAN_POINT('',(-25.7422751287225,-3.,98.6059254398751));
#5779=CARTESIAN_POINT('Origin',(-24.6422751287225,-3.,98.6059254398751));
#5780=CARTESIAN_POINT('',(-25.7422751287225,-4.,98.6059254398751));
#5781=CARTESIAN_POINT('',(-25.7422751287225,-4.,98.6059254398751));
#5782=CARTESIAN_POINT('Origin',(-24.6422751287225,-4.,98.6059254398751));
#5783=CARTESIAN_POINT('Origin',(28.5450224208979,-4.,108.02799088316));
#5784=CARTESIAN_POINT('',(27.4450224208979,-3.,108.02799088316));
#5785=CARTESIAN_POINT('Origin',(28.5450224208979,-3.,108.02799088316));
#5786=CARTESIAN_POINT('',(27.4450224208979,-4.,108.02799088316));
#5787=CARTESIAN_POINT('',(27.4450224208979,-4.,108.02799088316));
#5788=CARTESIAN_POINT('Origin',(28.5450224208979,-4.,108.02799088316));
#5789=CARTESIAN_POINT('Origin',(23.9595659283167,-4.,97.584178916323));
#5790=CARTESIAN_POINT('',(22.8595659283167,-3.,97.584178916323));
#5791=CARTESIAN_POINT('Origin',(23.9595659283167,-3.,97.584178916323));
#5792=CARTESIAN_POINT('',(22.8595659283167,-4.,97.584178916323));
#5793=CARTESIAN_POINT('',(22.8595659283167,-4.,97.584178916323));
#5794=CARTESIAN_POINT('Origin',(23.9595659283167,-4.,97.584178916323));
#5795=CARTESIAN_POINT('Origin',(-28.7847580111699,-4.,109.233223083803));
#5796=CARTESIAN_POINT('',(-29.8847580111699,-3.,109.233223083803));
#5797=CARTESIAN_POINT('Origin',(-28.7847580111699,-3.,109.233223083803));
#5798=CARTESIAN_POINT('',(-29.8847580111699,-4.,109.233223083803));
#5799=CARTESIAN_POINT('',(-29.8847580111699,-4.,109.233223083803));
#5800=CARTESIAN_POINT('Origin',(-28.7847580111699,-4.,109.233223083803));
#5801=CARTESIAN_POINT('Origin',(-5.09918507322789,-4.,143.1171661682));
#5802=CARTESIAN_POINT('',(-6.19918507322789,-3.,143.1171661682));
#5803=CARTESIAN_POINT('Origin',(-5.09918507322789,-3.,143.1171661682));
#5804=CARTESIAN_POINT('',(-6.19918507322789,-4.,143.1171661682));
#5805=CARTESIAN_POINT('',(-6.19918507322789,-4.,143.1171661682));
#5806=CARTESIAN_POINT('Origin',(-5.09918507322789,-4.,143.1171661682));
#5807=CARTESIAN_POINT('Origin',(0.,-4.,114.33240815703));
#5808=CARTESIAN_POINT('Origin',(0.,-3.,114.33240815703));
#6728=UNCERTAINTY_MEASURE_WITH_UNIT(LENGTH_MEASURE(0.01),#6754,
'DISTANCE_ACCURACY_VALUE',
'Maximum model space distance between geometric entities at asserted c
onnectivities');
#6738=UNCERTAINTY_MEASURE_WITH_UNIT(LENGTH_MEASURE(0.01),#6754,
'DISTANCE_ACCURACY_VALUE',
'Maximum model space distance between geometric entities at asserted c
onnectivities');
#6743=(
GEOMETRIC_REPRESENTATION_CONTEXT(3)
GLOBAL_UNCERTAINTY_ASSIGNED_CONTEXT((#6728))
GLOBAL_UNIT_ASSIGNED_CONTEXT((#6754,#6756,#6757))
REPRESENTATION_CONTEXT('','3D')
);
#6753=(
GEOMETRIC_REPRESENTATION_CONTEXT(3)
GLOBAL_UNCERTAINTY_ASSIGNED_CONTEXT((#6738))
GLOBAL_UNIT_ASSIGNED_CONTEXT((#6754,#6756,#6757))
REPRESENTATION_CONTEXT('','3D')
);
#6754=(
LENGTH_UNIT()
NAMED_UNIT(*)
SI_UNIT(.MILLI.,.METRE.)
);
#6756=(
NAMED_UNIT(*)
PLANE_ANGLE_UNIT()
SI_UNIT($,.RADIAN.)
);
#6757=(
NAMED_UNIT(*)
SI_UNIT($,.STERADIAN.)
SOLID_ANGLE_UNIT()
);
#6762=SHAPE_DEFINITION_REPRESENTATION(#6776,#6803);
#6776=PRODUCT_DEFINITION_SHAPE('',$,#6818);
#6803=SHAPE_REPRESENTATION('',(#3960),#6743);
#6813=PRODUCT_DEFINITION_CONTEXT('part definition',#6857,'design');
#6818=PRODUCT_DEFINITION('Front_Plate','Front_Plate',#6832,#6813);
#6832=PRODUCT_DEFINITION_FORMATION('',$,#6863);
#6857=APPLICATION_CONTEXT(
'Core Data for Automotive Mechanical Design Process');
#6858=PRODUCT_CONTEXT('part definition',#6857,'mechanical');
#6863=PRODUCT('Front_Plate','Front_Plate',$,(#6858));
#6929=COLOUR_RGB('Off White',0.89,0.88,0.83);
#6930=FILL_AREA_STYLE_COLOUR('',#6929);
#6931=FILL_AREA_STYLE('',(#6930));
#6932=SURFACE_STYLE_FILL_AREA(#6931);
#6933=SURFACE_SIDE_STYLE('',(#6932));
#6934=SURFACE_STYLE_USAGE(.BOTH.,#6933);
#6935=PRESENTATION_STYLE_ASSIGNMENT((#6934));
ENDSEC;
END-ISO-10303-21;
